ISO-10303-21;
HEADER;
/* Generated by software containing ST-Developer
 * from STEP Tools, Inc. (www.steptools.com) 
 */

FILE_DESCRIPTION(
/* description */ (''),
/* implementation_level */ '2;1');

FILE_NAME(
/* name */ '07_Mechanical_Seal_Carbon_Head.step',
/* time_stamp */ '2026-10-26T04:15:57-07:00',
/* author */ (''),
/* organization */ (''),
/* preprocessor_version */ 'ST-DEVELOPER v20.2',
/* originating_system */ 'Autodesk Translation Framework v15.15.0.0',
/* authorisation */ '');

FILE_SCHEMA (('AUTOMOTIVE_DESIGN { 1 0 10303 214 3 1 1 }'));
ENDSEC;

DATA;
#10=MECHANICAL_DESIGN_GEOMETRIC_PRESENTATION_REPRESENTATION('',(#458),#55737);
#374=CONICAL_SURFACE('',#29145,17.75,0.785398163397448);
#375=CONICAL_SURFACE('',#29158,17.5,0.785398163397449);
#418=SHAPE_REPRESENTATION_RELATIONSHIP('SRR','None',#55827,#438);
#438=ADVANCED_BREP_SHAPE_REPRESENTATION('',(#478),#55723);
#458=STYLED_ITEM('',(#55998),#478);
#478=MANIFOLD_SOLID_BREP('Body1',#27227);
#696=FACE_BOUND('',#9495,.T.);
#697=FACE_BOUND('',#9498,.T.);
#698=FACE_BOUND('',#9502,.T.);
#699=FACE_BOUND('',#9505,.T.);
#1387=PLANE('',#29151);
#1388=PLANE('',#29156);
#1389=PLANE('',#29161);
#1390=PLANE('',#29165);
#3326=LINE('',#45189,#5697);
#3327=LINE('',#45195,#5698);
#3328=LINE('',#45204,#5699);
#3329=LINE('',#45210,#5700);
#3330=LINE('',#45214,#5701);
#3331=LINE('',#45220,#5702);
#5697=VECTOR('',#34914,17.75);
#5698=VECTOR('',#34921,18.);
#5699=VECTOR('',#34932,10.);
#5700=VECTOR('',#34941,17.5);
#5701=VECTOR('',#34946,16.);
#5702=VECTOR('',#34953,13.);
#6685=CYLINDRICAL_SURFACE('',#29149,18.);
#6686=CYLINDRICAL_SURFACE('',#29153,10.);
#6687=CYLINDRICAL_SURFACE('',#29159,16.);
#6688=CYLINDRICAL_SURFACE('',#29163,13.);
#7831=FACE_OUTER_BOUND('',#9492,.T.);
#7832=FACE_OUTER_BOUND('',#9493,.T.);
#7833=FACE_OUTER_BOUND('',#9494,.T.);
#7834=FACE_OUTER_BOUND('',#9496,.T.);
#7835=FACE_OUTER_BOUND('',#9497,.T.);
#7836=FACE_OUTER_BOUND('',#9499,.T.);
#7837=FACE_OUTER_BOUND('',#9500,.T.);
#7838=FACE_OUTER_BOUND('',#9501,.T.);
#7839=FACE_OUTER_BOUND('',#9503,.T.);
#7840=FACE_OUTER_BOUND('',#9504,.T.);
#9492=EDGE_LOOP('',(#22926,#22927,#22928,#22929,#22930));
#9493=EDGE_LOOP('',(#22931,#22932,#22933,#22934,#22935));
#9494=EDGE_LOOP('',(#22936));
#9495=EDGE_LOOP('',(#22937));
#9496=EDGE_LOOP('',(#22938,#22939,#22940,#22941));
#9497=EDGE_LOOP('',(#22942));
#9498=EDGE_LOOP('',(#22943));
#9499=EDGE_LOOP('',(#22944,#22945,#22946,#22947));
#9500=EDGE_LOOP('',(#22948,#22949,#22950,#22951));
#9501=EDGE_LOOP('',(#22952));
#9502=EDGE_LOOP('',(#22953));
#9503=EDGE_LOOP('',(#22954,#22955,#22956,#22957));
#9504=EDGE_LOOP('',(#22958));
#9505=EDGE_LOOP('',(#22959));
#10756=CIRCLE('',#29146,17.5);
#10757=CIRCLE('',#29147,18.);
#10758=CIRCLE('',#29148,18.);
#10759=CIRCLE('',#29150,18.);
#10760=CIRCLE('',#29152,16.);
#10761=CIRCLE('',#29154,10.);
#10762=CIRCLE('',#29155,10.);
#10763=CIRCLE('',#29157,17.);
#10764=CIRCLE('',#29160,16.);
#10765=CIRCLE('',#29162,13.);
#10766=CIRCLE('',#29164,13.);
#13067=VERTEX_POINT('',#45186);
#13068=VERTEX_POINT('',#45188);
#13069=VERTEX_POINT('',#45190);
#13070=VERTEX_POINT('',#45194);
#13071=VERTEX_POINT('',#45198);
#13072=VERTEX_POINT('',#45201);
#13073=VERTEX_POINT('',#45203);
#13074=VERTEX_POINT('',#45207);
#13075=VERTEX_POINT('',#45212);
#13076=VERTEX_POINT('',#45216);
#13077=VERTEX_POINT('',#45219);
#16467=EDGE_CURVE('',#13067,#13067,#10756,.T.);
#16468=EDGE_CURVE('',#13067,#13068,#3326,.T.);
#16469=EDGE_CURVE('',#13068,#13069,#10757,.T.);
#16470=EDGE_CURVE('',#13069,#13068,#10758,.T.);
#16471=EDGE_CURVE('',#13069,#13070,#3327,.T.);
#16472=EDGE_CURVE('',#13070,#13070,#10759,.T.);
#16473=EDGE_CURVE('',#13071,#13071,#10760,.T.);
#16474=EDGE_CURVE('',#13072,#13072,#10761,.T.);
#16475=EDGE_CURVE('',#13072,#13073,#3328,.T.);
#16476=EDGE_CURVE('',#13073,#13073,#10762,.T.);
#16477=EDGE_CURVE('',#13074,#13074,#10763,.T.);
#16478=EDGE_CURVE('',#13070,#13074,#3329,.T.);
#16479=EDGE_CURVE('',#13075,#13075,#10764,.T.);
#16480=EDGE_CURVE('',#13075,#13071,#3330,.T.);
#16481=EDGE_CURVE('',#13076,#13076,#10765,.T.);
#16482=EDGE_CURVE('',#13076,#13077,#3331,.T.);
#16483=EDGE_CURVE('',#13077,#13077,#10766,.T.);
#22926=ORIENTED_EDGE('',*,*,#16467,.T.);
#22927=ORIENTED_EDGE('',*,*,#16468,.T.);
#22928=ORIENTED_EDGE('',*,*,#16469,.T.);
#22929=ORIENTED_EDGE('',*,*,#16470,.T.);
#22930=ORIENTED_EDGE('',*,*,#16468,.F.);
#22931=ORIENTED_EDGE('',*,*,#16469,.F.);
#22932=ORIENTED_EDGE('',*,*,#16470,.F.);
#22933=ORIENTED_EDGE('',*,*,#16471,.T.);
#22934=ORIENTED_EDGE('',*,*,#16472,.T.);
#22935=ORIENTED_EDGE('',*,*,#16471,.F.);
#22936=ORIENTED_EDGE('',*,*,#16467,.F.);
#22937=ORIENTED_EDGE('',*,*,#16473,.F.);
#22938=ORIENTED_EDGE('',*,*,#16474,.T.);
#22939=ORIENTED_EDGE('',*,*,#16475,.T.);
#22940=ORIENTED_EDGE('',*,*,#16476,.F.);
#22941=ORIENTED_EDGE('',*,*,#16475,.F.);
#22942=ORIENTED_EDGE('',*,*,#16477,.F.);
#22943=ORIENTED_EDGE('',*,*,#16476,.T.);
#22944=ORIENTED_EDGE('',*,*,#16472,.F.);
#22945=ORIENTED_EDGE('',*,*,#16478,.T.);
#22946=ORIENTED_EDGE('',*,*,#16477,.T.);
#22947=ORIENTED_EDGE('',*,*,#16478,.F.);
#22948=ORIENTED_EDGE('',*,*,#16479,.F.);
#22949=ORIENTED_EDGE('',*,*,#16480,.T.);
#22950=ORIENTED_EDGE('',*,*,#16473,.T.);
#22951=ORIENTED_EDGE('',*,*,#16480,.F.);
#22952=ORIENTED_EDGE('',*,*,#16479,.T.);
#22953=ORIENTED_EDGE('',*,*,#16481,.F.);
#22954=ORIENTED_EDGE('',*,*,#16481,.T.);
#22955=ORIENTED_EDGE('',*,*,#16482,.T.);
#22956=ORIENTED_EDGE('',*,*,#16483,.F.);
#22957=ORIENTED_EDGE('',*,*,#16482,.F.);
#22958=ORIENTED_EDGE('',*,*,#16483,.T.);
#22959=ORIENTED_EDGE('',*,*,#16474,.F.);
#26655=ADVANCED_FACE('',(#7831),#374,.T.);
#26656=ADVANCED_FACE('',(#7832),#6685,.T.);
#26657=ADVANCED_FACE('',(#7833,#696),#1387,.T.);
#26658=ADVANCED_FACE('',(#7834),#6686,.F.);
#26659=ADVANCED_FACE('',(#7835,#697),#1388,.T.);
#26660=ADVANCED_FACE('',(#7836),#375,.T.);
#26661=ADVANCED_FACE('',(#7837),#6687,.T.);
#26662=ADVANCED_FACE('',(#7838,#698),#1389,.T.);
#26663=ADVANCED_FACE('',(#7839),#6688,.F.);
#26664=ADVANCED_FACE('',(#7840,#699),#1390,.T.);
#27227=CLOSED_SHELL('',(#26655,#26656,#26657,#26658,#26659,#26660,#26661,
#26662,#26663,#26664));
#29144=AXIS2_PLACEMENT_3D('',#45184,#34908,#34909);
#29145=AXIS2_PLACEMENT_3D('',#45185,#34910,#34911);
#29146=AXIS2_PLACEMENT_3D('',#45187,#34912,#34913);
#29147=AXIS2_PLACEMENT_3D('',#45191,#34915,#34916);
#29148=AXIS2_PLACEMENT_3D('',#45192,#34917,#34918);
#29149=AXIS2_PLACEMENT_3D('',#45193,#34919,#34920);
#29150=AXIS2_PLACEMENT_3D('',#45196,#34922,#34923);
#29151=AXIS2_PLACEMENT_3D('',#45197,#34924,#34925);
#29152=AXIS2_PLACEMENT_3D('',#45199,#34926,#34927);
#29153=AXIS2_PLACEMENT_3D('',#45200,#34928,#34929);
#29154=AXIS2_PLACEMENT_3D('',#45202,#34930,#34931);
#29155=AXIS2_PLACEMENT_3D('',#45205,#34933,#34934);
#29156=AXIS2_PLACEMENT_3D('',#45206,#34935,#34936);
#29157=AXIS2_PLACEMENT_3D('',#45208,#34937,#34938);
#29158=AXIS2_PLACEMENT_3D('',#45209,#34939,#34940);
#29159=AXIS2_PLACEMENT_3D('',#45211,#34942,#34943);
#29160=AXIS2_PLACEMENT_3D('',#45213,#34944,#34945);
#29161=AXIS2_PLACEMENT_3D('',#45215,#34947,#34948);
#29162=AXIS2_PLACEMENT_3D('',#45217,#34949,#34950);
#29163=AXIS2_PLACEMENT_3D('',#45218,#34951,#34952);
#29164=AXIS2_PLACEMENT_3D('',#45221,#34954,#34955);
#29165=AXIS2_PLACEMENT_3D('',#45222,#34956,#34957);
#34908=DIRECTION('axis',(0.,0.,1.));
#34909=DIRECTION('refdir',(1.,0.,0.));
#34910=DIRECTION('center_axis',(-1.,0.,0.));
#34911=DIRECTION('ref_axis',(0.,-1.,0.));
#34912=DIRECTION('center_axis',(-1.,0.,0.));
#34913=DIRECTION('ref_axis',(0.,-1.,0.));
#34914=DIRECTION('',(-0.707106781186547,0.707106781186547,8.65956056235493E-17));
#34915=DIRECTION('center_axis',(1.,0.,0.));
#34916=DIRECTION('ref_axis',(0.,-1.,0.));
#34917=DIRECTION('center_axis',(1.,0.,0.));
#34918=DIRECTION('ref_axis',(0.,-1.,0.));
#34919=DIRECTION('center_axis',(1.,0.,0.));
#34920=DIRECTION('ref_axis',(0.,1.,0.));
#34921=DIRECTION('',(-1.,0.,0.));
#34922=DIRECTION('center_axis',(1.,0.,0.));
#34923=DIRECTION('ref_axis',(0.,0.,-1.));
#34924=DIRECTION('center_axis',(1.,0.,0.));
#34925=DIRECTION('ref_axis',(0.,0.,-1.));
#34926=DIRECTION('center_axis',(1.,0.,0.));
#34927=DIRECTION('ref_axis',(0.,0.,-1.));
#34928=DIRECTION('center_axis',(1.,0.,0.));
#34929=DIRECTION('ref_axis',(0.,1.,0.));
#34930=DIRECTION('center_axis',(1.,0.,0.));
#34931=DIRECTION('ref_axis',(0.,0.,-1.));
#34932=DIRECTION('',(-1.,0.,0.));
#34933=DIRECTION('center_axis',(1.,0.,0.));
#34934=DIRECTION('ref_axis',(0.,0.,-1.));
#34935=DIRECTION('center_axis',(-1.,0.,0.));
#34936=DIRECTION('ref_axis',(0.,0.,1.));
#34937=DIRECTION('center_axis',(1.,0.,0.));
#34938=DIRECTION('ref_axis',(0.,0.,-1.));
#34939=DIRECTION('center_axis',(1.,0.,0.));
#34940=DIRECTION('ref_axis',(0.,1.,0.));
#34941=DIRECTION('',(-0.707106781186547,0.707106781186548,8.65956056235494E-17));
#34942=DIRECTION('center_axis',(1.,0.,0.));
#34943=DIRECTION('ref_axis',(0.,1.,0.));
#34944=DIRECTION('center_axis',(1.,0.,0.));
#34945=DIRECTION('ref_axis',(0.,0.,-1.));
#34946=DIRECTION('',(-1.,0.,0.));
#34947=DIRECTION('center_axis',(1.,0.,0.));
#34948=DIRECTION('ref_axis',(0.,0.,-1.));
#34949=DIRECTION('center_axis',(1.,0.,0.));
#34950=DIRECTION('ref_axis',(0.,0.,-1.));
#34951=DIRECTION('center_axis',(1.,0.,0.));
#34952=DIRECTION('ref_axis',(0.,1.,0.));
#34953=DIRECTION('',(-1.,0.,0.));
#34954=DIRECTION('center_axis',(1.,0.,0.));
#34955=DIRECTION('ref_axis',(0.,0.,-1.));
#34956=DIRECTION('center_axis',(1.,0.,0.));
#34957=DIRECTION('ref_axis',(0.,0.,-1.));
#45184=CARTESIAN_POINT('',(0.,0.,0.));
#45185=CARTESIAN_POINT('Origin',(16.75,0.,0.));
#45186=CARTESIAN_POINT('',(17.,17.5,-2.14313189850787E-15));
#45187=CARTESIAN_POINT('Origin',(17.,0.,0.));
#45188=CARTESIAN_POINT('',(16.5,18.,2.20436423846524E-15));
#45189=CARTESIAN_POINT('',(16.75,17.75,2.17374806848655E-15));
#45190=CARTESIAN_POINT('',(16.5,-18.,-2.20436423846524E-15));
#45191=CARTESIAN_POINT('Origin',(16.5,0.,0.));
#45192=CARTESIAN_POINT('Origin',(16.5,0.,0.));
#45193=CARTESIAN_POINT('Origin',(11.5,0.,0.));
#45194=CARTESIAN_POINT('',(6.,-18.,-2.20436423846524E-15));
#45195=CARTESIAN_POINT('',(11.5,-18.,-2.20436423846524E-15));
#45196=CARTESIAN_POINT('Origin',(6.,0.,0.));
#45197=CARTESIAN_POINT('Origin',(17.,16.,0.));
#45198=CARTESIAN_POINT('',(17.,-16.,-1.95943487863577E-15));
#45199=CARTESIAN_POINT('Origin',(17.,0.,0.));
#45200=CARTESIAN_POINT('Origin',(11.,0.,0.));
#45201=CARTESIAN_POINT('',(17.,-10.,-1.22464679914735E-15));
#45202=CARTESIAN_POINT('Origin',(17.,0.,0.));
#45203=CARTESIAN_POINT('',(5.,-10.,-1.22464679914735E-15));
#45204=CARTESIAN_POINT('',(11.,-10.,-1.22464679914735E-15));
#45205=CARTESIAN_POINT('Origin',(5.,0.,0.));
#45206=CARTESIAN_POINT('Origin',(5.,17.,0.));
#45207=CARTESIAN_POINT('',(5.,-17.,-2.0818995585505E-15));
#45208=CARTESIAN_POINT('Origin',(5.,0.,0.));
#45209=CARTESIAN_POINT('Origin',(5.5,0.,0.));
#45210=CARTESIAN_POINT('',(5.5,-17.5,-2.14313189850787E-15));
#45211=CARTESIAN_POINT('Origin',(19.5,0.,0.));
#45212=CARTESIAN_POINT('',(22.,-16.,-1.95943487863577E-15));
#45213=CARTESIAN_POINT('Origin',(22.,0.,0.));
#45214=CARTESIAN_POINT('',(19.5,-16.,-1.95943487863577E-15));
#45215=CARTESIAN_POINT('Origin',(22.,13.,0.));
#45216=CARTESIAN_POINT('',(22.,-13.,-1.59204083889156E-15));
#45217=CARTESIAN_POINT('Origin',(22.,0.,0.));
#45218=CARTESIAN_POINT('Origin',(19.5,0.,0.));
#45219=CARTESIAN_POINT('',(17.,-13.,-1.59204083889156E-15));
#45220=CARTESIAN_POINT('',(19.5,-13.,-1.59204083889156E-15));
#45221=CARTESIAN_POINT('Origin',(17.,0.,0.));
#45222=CARTESIAN_POINT('Origin',(17.,10.,0.));
#55701=UNCERTAINTY_MEASURE_WITH_UNIT(LENGTH_MEASURE(0.01),#55738,
'DISTANCE_ACCURACY_VALUE',
'Maximum model space distance between geometric entities at asserted c
onnectivities');
#55715=UNCERTAINTY_MEASURE_WITH_UNIT(LENGTH_MEASURE(0.01),#55738,
'DISTANCE_ACCURACY_VALUE',
'Maximum model space distance between geometric entities at asserted c
onnectivities');
#55723=(
GEOMETRIC_REPRESENTATION_CONTEXT(3)
GLOBAL_UNCERTAINTY_ASSIGNED_CONTEXT((#55701))
GLOBAL_UNIT_ASSIGNED_CONTEXT((#55738,#55740,#55741))
REPRESENTATION_CONTEXT('','3D')
);
#55737=(
GEOMETRIC_REPRESENTATION_CONTEXT(3)
GLOBAL_UNCERTAINTY_ASSIGNED_CONTEXT((#55715))
GLOBAL_UNIT_ASSIGNED_CONTEXT((#55738,#55740,#55741))
REPRESENTATION_CONTEXT('','3D')
);
#55738=(
LENGTH_UNIT()
NAMED_UNIT(*)
SI_UNIT(.MILLI.,.METRE.)
);
#55740=(
NAMED_UNIT(*)
PLANE_ANGLE_UNIT()
SI_UNIT($,.RADIAN.)
);
#55741=(
NAMED_UNIT(*)
SI_UNIT($,.STERADIAN.)
SOLID_ANGLE_UNIT()
);
#55749=SHAPE_DEFINITION_REPRESENTATION(#55770,#55827);
#55770=PRODUCT_DEFINITION_SHAPE('',$,#55849);
#55827=SHAPE_REPRESENTATION('',(#29144),#55723);
#55841=PRODUCT_DEFINITION_CONTEXT('part definition',#55906,'design');
#55849=PRODUCT_DEFINITION('2026-10-26-00-34-23-727',
'07_Mechanical_Seal_Carbon_Head',#55870,#55841);
#55870=PRODUCT_DEFINITION_FORMATION('',$,#55915);
#55906=APPLICATION_CONTEXT(
'Core Data for Automotive Mechanical Design Process');
#55907=PRODUCT_CONTEXT('part definition',#55906,'mechanical');
#55915=PRODUCT('2026-10-26-00-34-23-727',
'07_Mechanical_Seal_Carbon_Head',$,(#55907));
#55992=COLOUR_RGB('Black',0.12,0.14,0.17);
#55993=FILL_AREA_STYLE_COLOUR('',#55992);
#55994=FILL_AREA_STYLE('',(#55993));
#55995=SURFACE_STYLE_FILL_AREA(#55994);
#55996=SURFACE_SIDE_STYLE('',(#55995));
#55997=SURFACE_STYLE_USAGE(.BOTH.,#55996);
#55998=PRESENTATION_STYLE_ASSIGNMENT((#55997));
ENDSEC;
END-ISO-10303-21;
